ISO-10303-21;
HEADER;
FILE_DESCRIPTION (('STEP AP203'),
    '1' );
FILE_NAME ('1602p_c_33.step',
    '2026-10-31T14:11:27',
    ( '' ),
    ( '' ),
    'SwSTEP 2.0',
    'SolidWorks 2024',
    '' );
FILE_SCHEMA (( 'AUTOMOTIVE_DESIGN' ));
ENDSEC;

DATA;
#38=CARTESIAN_POINT ( 'NONE',  ( -18.05391955182270181, 22.49081825942809942, -4.900728725074969882E-15 ) ) ;
#74=AXIS2_PLACEMENT_3D ( 'NONE', #22405, #17064, #15522 ) ;
#190=DIRECTION ( 'NONE',  ( -0.2306359803922032603, -0.9730401042858035643, 4.741332172907965995E-18 ) ) ;
#238=VERTEX_POINT ( 'NONE', #344 ) ;
#283=DIRECTION ( 'NONE',  ( 0.000000000000000000, -2.755911201911430512E-15, -1.000000000000000000 ) ) ;
#330=ORIENTED_EDGE ( 'NONE', *, *, #2152, .T. ) ;
#333=CYLINDRICAL_SURFACE ( 'NONE', #19089, 2.066999999999997062 ) ;
#344=CARTESIAN_POINT ( 'NONE',  ( -19.80660126203780180, 15.09635365252939998, -2.500000000000000000 ) ) ;
#415=DIRECTION ( 'NONE',  ( 1.000000000000000000, 0.000000000000000000, 0.000000000000000000 ) ) ;
#417=FACE_OUTER_BOUND ( 'NONE', #3164, .T. ) ;
#436=CARTESIAN_POINT ( 'NONE',  ( -0.5391976746782171093, 18.33937061236849075, -4.999999999999997335 ) ) ;
#445=AXIS2_PLACEMENT_3D ( 'NONE', #15992, #21341, #4955 ) ;
#457=DIRECTION ( 'NONE',  ( 0.9730401042858035643, -0.2306359803922028717, 2.025546614365803772E-16 ) ) ;
#484=CARTESIAN_POINT ( 'NONE',  ( -11.24263882182209962, 20.87636639668270178, -2.982050098520939832E-15 ) ) ;
#583=CARTESIAN_POINT ( 'NONE',  ( -6.134178274321590685, 19.66552749962360025, -1.543041128605420056E-15 ) ) ;
#587=VERTEX_POINT ( 'NONE', #21457 ) ;
#597=ORIENTED_EDGE ( 'NONE', *, *, #2152, .F. ) ;
#599=CARTESIAN_POINT ( 'NONE',  ( -2.384285517815838862, 10.55504977808206846, -9.087704672992351837E-16 ) ) ;
#606=ORIENTED_EDGE ( 'NONE', *, *, #3941, .F. ) ;
#620=DIRECTION ( 'NONE',  ( 0.2306359803922031215, 0.9730401042858034533, -4.741332172907939802E-18 ) ) ;
#636=LINE ( 'NONE', #7897, #13374 ) ;
#754=ORIENTED_EDGE ( 'NONE', *, *, #12897, .F. ) ;
#791=AXIS2_PLACEMENT_3D ( 'NONE', #18120, #19903, #8979 ) ;
#796=PRODUCT_DEFINITION_FORMATION_WITH_SPECIFIED_SOURCE ( 'ANY', '', #1104, .NOT_KNOWN. ) ;
#822=DIRECTION ( 'NONE',  ( -0.9730401042858036753, 0.2306359803922031493, -2.740969466505752002E-16 ) ) ;
#826=AXIS2_PLACEMENT_3D ( 'NONE', #11250, #2075, #14665 ) ;
#851=VERTEX_POINT ( 'NONE', #22856 ) ;
#863=CARTESIAN_POINT ( 'NONE',  ( -25.65326162860803194, 22.49081825942809942, 2.499999999999996891 ) ) ;
#904=DIRECTION ( 'NONE',  ( 0.9730401042858035643, -0.2306359803922028717, 2.740969466505749044E-16 ) ) ;
#914=CYLINDRICAL_SURFACE ( 'NONE', #8817, 3.500000000000000444 ) ;
#985=PLANE ( 'NONE',  #9370 ) ;
#1104=PRODUCT ( '1602p_c_33', '1602p_c_33', '', ( #22706 ) ) ;
#1179=EDGE_CURVE ( 'NONE', #238, #12726, #5208, .T. ) ;
#1190=CARTESIAN_POINT ( 'NONE',  ( -3.458317987535632909, 19.03127855354509990, 7.999999999999996447 ) ) ;
#1283=VECTOR ( 'NONE', #11605, 1000.000000000000114 ) ;
#1286=TOROIDAL_SURFACE ( 'NONE', #20269, 5.000000000000000000, 3.000000000000000000 ) ;
#1307=VERTEX_POINT ( 'NONE', #14884 ) ;
#1319=EDGE_CURVE ( 'NONE', #11373, #16606, #10165, .T. ) ;
#1333=DIRECTION ( 'NONE',  ( 0.2306359803922037599, 0.9730401042858033422, -4.741332172908110825E-18 ) ) ;
#1335=FACE_OUTER_BOUND ( 'NONE', #19472, .T. ) ;
#1340=EDGE_CURVE ( 'NONE', #851, #22662, #11305, .T. ) ;
#1358=( NAMED_UNIT ( * ) PLANE_ANGLE_UNIT ( ) SI_UNIT ( $, .RADIAN. ) );
#1367=CYLINDRICAL_SURFACE ( 'NONE', #4640, 3.500000000000000444 ) ;
#1400=AXIS2_PLACEMENT_3D ( 'NONE', #2648, #2997, #22823 ) ;
#1481=DIRECTION ( 'NONE',  ( 0.9730401042858036753, -0.2306359803922031493, 2.740969466505752002E-16 ) ) ;
#1511=DIRECTION ( 'NONE',  ( 2.086281924601080239E-16, 1.946516371809877606E-18, -1.000000000000000000 ) ) ;
#1587=FACE_OUTER_BOUND ( 'NONE', #17448, .T. ) ;
#1627=FACE_OUTER_BOUND ( 'NONE', #13311, .T. ) ;
#1628=ORIENTED_EDGE ( 'NONE', *, *, #9085, .T. ) ;
#1652=AXIS2_PLACEMENT_3D ( 'NONE', #2656, #2183, #4339 ) ;
#1868=ORIENTED_EDGE ( 'NONE', *, *, #3956, .T. ) ;
#1935=DIRECTION ( 'NONE',  ( -0.9730401042858036753, 0.2306359803922031493, -2.740969466505752002E-16 ) ) ;
#2005=EDGE_CURVE ( 'NONE', #6113, #4832, #20901, .T. ) ;
#2012=( LENGTH_UNIT ( ) NAMED_UNIT ( * ) SI_UNIT ( .MILLI., .METRE. ) );
#2053=AXIS2_PLACEMENT_3D ( 'NONE', #16011, #21699, #2221 ) ;
#2075=DIRECTION ( 'NONE',  ( -0.9730401042858036753, 0.2306359803922031493, -2.740969466505752002E-16 ) ) ;
#2101=ORIENTED_EDGE ( 'NONE', *, *, #20735, .F. ) ;
#2120=LINE ( 'NONE', #9376, #3895 ) ;
#2129=DIRECTION ( 'NONE',  ( 0.9730401042858035643, -0.2306359803922028717, 2.740969466505749044E-16 ) ) ;
#2152=EDGE_CURVE ( 'NONE', #11903, #7064, #10865, .T. ) ;
#2168=ORIENTED_EDGE ( 'NONE', *, *, #6785, .T. ) ;
#2180=DIRECTION ( 'NONE',  ( -2.656137997592320068E-16, 6.783012436524469908E-17, 1.000000000000000000 ) ) ;
#2183=DIRECTION ( 'NONE',  ( -1.248400535696349791E-16, 3.446306084657144903E-17, 1.000000000000000000 ) ) ;
#2192=ORIENTED_EDGE ( 'NONE', *, *, #1319, .T. ) ;
#2196=VECTOR ( 'NONE', #14550, 1000.000000000000114 ) ;
#2221=DIRECTION ( 'NONE',  ( -0.2306359803922030105, -0.9730401042858034533, 0.000000000000000000 ) ) ;
#2242=DIRECTION ( 'NONE',  ( -0.9730401042858036753, 0.2306359803922031493, -2.740969466505752002E-16 ) ) ;
#2252=ORIENTED_EDGE ( 'NONE', *, *, #12127, .T. ) ;
#2274=ORIENTED_EDGE ( 'NONE', *, *, #3323, .T. ) ;
#2318=EDGE_LOOP ( 'NONE', ( #12968, #6059, #17001 ) ) ;
#2365=VECTOR ( 'NONE', #12130, 999.9999999999998863 ) ;
#2403=ORIENTED_EDGE ( 'NONE', *, *, #12336, .T. ) ;
#2411=AXIS2_PLACEMENT_3D ( 'NONE', #38, #9200, #14303 ) ;
#2423=AXIS2_PLACEMENT_3D ( 'NONE', #16664, #22929, #18596 ) ;
#2502=ORIENTED_EDGE ( 'NONE', *, *, #10974, .T. ) ;
#2543=VECTOR ( 'NONE', #10216, 1000.000000000000114 ) ;
#2546=CARTESIAN_POINT ( 'NONE',  ( -0.5391976746782148888, 18.33937061236850141, 3.301631463538509622E-17 ) ) ;
#2558=ORIENTED_EDGE ( 'NONE', *, *, #1179, .F. ) ;
#2560=AXIS2_PLACEMENT_3D ( 'NONE', #12570, #9240, #16122 ) ;
#2569=CARTESIAN_POINT ( 'NONE',  ( 0.000000000000000000, 0.000000000000000000, 0.000000000000000000 ) ) ;
#2591=VERTEX_POINT ( 'NONE', #18592 ) ;
#2642=ORIENTED_EDGE ( 'NONE', *, *, #3233, .F. ) ;
#2648=CARTESIAN_POINT ( 'NONE',  ( -3.458317987535629801, 19.03127855354509990, -7.892745253163399067E-16 ) ) ;
#2656=CARTESIAN_POINT ( 'NONE',  ( -20.00000000397270128, 22.95208919256889857, -2.500000000000000000 ) ) ;
#2701=DIRECTION ( 'NONE',  ( -0.2306359803922027885, -0.9730401042858034533, 4.741332172908048425E-18 ) ) ;
#2748=AXIS2_PLACEMENT_3D ( 'NONE', #4163, #822, #7848 ) ;
#2779=CARTESIAN_POINT ( 'NONE',  ( -16.30123784160759826, 29.88528286632680064, -2.500000000000000000 ) ) ;
#2845=EDGE_CURVE ( 'NONE', #16606, #19785, #12025, .T. ) ;
#2871=EDGE_CURVE ( 'NONE', #5508, #6113, #12853, .T. ) ;
#2997=DIRECTION ( 'NONE',  ( 0.9730401042858036753, -0.2306359803922031493, 2.740969466505752002E-16 ) ) ;
#3030=LINE ( 'NONE', #10535, #2196 ) ;
#3042=CARTESIAN_POINT ( 'NONE',  ( -3.458317987535629801, 19.03127855354509990, -7.892745253163399067E-16 ) ) ;
#3050=APPLICATION_CONTEXT ( 'configuration controlled 3d designs of mechanical parts and assemblies' ) ;
#3076=EDGE_LOOP ( 'NONE', ( #22913, #12364, #4860, #11218, #15084 ) ) ;
#3164=EDGE_LOOP ( 'NONE', ( #330, #12431, #18994, #2642 ) ) ;
#3233=EDGE_CURVE ( 'NONE', #11903, #4956, #8773, .T. ) ;
#3245=DIRECTION ( 'NONE',  ( -4.302370362259564196E-33, 3.446306084657139973E-17, 1.000000000000000000 ) ) ;
#3308=AXIS2_PLACEMENT_3D ( 'NONE', #13116, #1935, #620 ) ;
#3323=EDGE_CURVE ( 'NONE', #7064, #11903, #23374, .T. ) ;
#3388=AXIS2_PLACEMENT_3D ( 'NONE', #10636, #19297, #10287 ) ;
#3439=CIRCLE ( 'NONE', #826, 4.999999999999997335 ) ;
#3500=AXIS2_PLACEMENT_3D ( 'NONE', #3042, #1481, #4716 ) ;
#3538=ORIENTED_EDGE ( 'NONE', *, *, #12897, .T. ) ;
#3617=EDGE_CURVE ( 'NONE', #16606, #18892, #9964, .T. ) ;
#3694=ADVANCED_FACE ( 'NONE', ( #17423 ), #1367, .F. ) ;
#3735=FACE_OUTER_BOUND ( 'NONE', #9335, .T. ) ;
#3867=AXIS2_PLACEMENT_3D ( 'NONE', #13480, #14905, #8144 ) ;
#3873=EDGE_CURVE ( 'NONE', #15418, #4956, #12622, .T. ) ;
#3881=EDGE_CURVE ( 'NONE', #10728, #19785, #3439, .T. ) ;
#3895=VECTOR ( 'NONE', #14828, 1000.000000000000114 ) ;
#3941=EDGE_CURVE ( 'NONE', #17240, #10728, #14109, .T. ) ;
#3956=EDGE_CURVE ( 'NONE', #587, #4833, #636, .T. ) ;
#4006=DIRECTION ( 'NONE',  ( -2.656137997592320068E-16, 6.783012436524469908E-17, 1.000000000000000000 ) ) ;
#4031=ORIENTED_EDGE ( 'NONE', *, *, #7331, .F. ) ;
#4091=FACE_OUTER_BOUND ( 'NONE', #2318, .T. ) ;
#4162=ORIENTED_EDGE ( 'NONE', *, *, #19946, .T. ) ;
#4163=CARTESIAN_POINT ( 'NONE',  ( -18.05391955182270181, 22.49081825942809942, -4.900728725074969882E-15 ) ) ;
#4188=EDGE_LOOP ( 'NONE', ( #7620, #21259, #10987, #15430, #6888 ) ) ;
#4207=DIRECTION ( 'NONE',  ( -0.9730401042858036753, 0.2306359803922031493, -2.740969466505752002E-16 ) ) ;
#4269=APPLICATION_CONTEXT ( 'configuration controlled 3d designs of mechanical parts and assemblies' ) ;
#4288=EDGE_CURVE ( 'NONE', #21240, #238, #4662, .T. ) ;
#4307=CIRCLE ( 'NONE', #14169, 2.067000000000000615 ) ;
#4339=DIRECTION ( 'NONE',  ( -0.2306359803922030105, -0.9730401042858034533, 0.000000000000000000 ) ) ;
#4424=CONICAL_SURFACE ( 'NONE', #18865, 2.283500000000000529, 0.7853981633974476129 ) ;
#4446=CARTESIAN_POINT ( 'NONE',  ( -0.5391976746782192187, 18.33937061236849075, 4.999999999999997335 ) ) ;
#4478=CARTESIAN_POINT ( 'NONE',  ( -0.7498608572560920837, 18.38930330212339825, -2.632567431446439807E-17 ) ) ;
#4631=ORIENTED_EDGE ( 'NONE', *, *, #9826, .T. ) ;
#4640=AXIS2_PLACEMENT_3D ( 'NONE', #15867, #10544, #10659 ) ;
#4662=CIRCLE ( 'NONE', #17940, 7.599342076785325695 ) ;
#4716=DIRECTION ( 'NONE',  ( 0.2306359803922030938, 0.9730401042858035643, -4.741332172907964454E-18 ) ) ;
#4828=AXIS2_PLACEMENT_3D ( 'NONE', #12661, #6969, #23079 ) ;
#4832=VERTEX_POINT ( 'NONE', #7041 ) ;
#4833=VERTEX_POINT ( 'NONE', #21392 ) ;
#4849=EDGE_CURVE ( 'NONE', #17240, #11373, #20850, .T. ) ;
#4860=ORIENTED_EDGE ( 'NONE', *, *, #3941, .T. ) ;
#4955=DIRECTION ( 'NONE',  ( -0.2306359803922030105, -0.9730401042858034533, 0.000000000000000000 ) ) ;
#4956=VERTEX_POINT ( 'NONE', #15080 ) ;
#4966=ORIENTED_EDGE ( 'NONE', *, *, #13009, .T. ) ;
#4984=ORIENTED_EDGE ( 'NONE', *, *, #20099, .F. ) ;
#5031=CIRCLE ( 'NONE', #74, 8.000000000000000000 ) ;
#5202=ORIENTED_EDGE ( 'NONE', *, *, #2871, .T. ) ;
#5208=CIRCLE ( 'NONE', #3308, 7.999999999999998224 ) ;
#5237=VERTEX_POINT ( 'NONE', #17235 ) ;
#5412=AXIS2_PLACEMENT_3D ( 'NONE', #14668, #20261, #18481 ) ;
#5435=DIRECTION ( 'NONE',  ( 0.9730401042858035643, -0.2306359803922028717, -8.741838862554660940E-17 ) ) ;
#5459=CIRCLE ( 'NONE', #1652, 3.499999999999996891 ) ;
#5508=VERTEX_POINT ( 'NONE', #22604 ) ;
#5609=CARTESIAN_POINT ( 'NONE',  ( -18.05391955182270181, 22.49081825942809942, 2.500000000000000000 ) ) ;
#5759=EDGE_CURVE ( 'NONE', #6113, #4832, #21204, .T. ) ;
#5779=CARTESIAN_POINT ( 'NONE',  ( -0.7498608572560920837, 18.38930330212339825, -2.632567431446439807E-17 ) ) ;
#5827=CARTESIAN_POINT ( 'NONE',  ( -3.458317987535629801, 19.03127855354509990, -7.892745253163399067E-16 ) ) ;
#5879=FACE_OUTER_BOUND ( 'NONE', #19039, .T. ) ;
#6011=CARTESIAN_POINT ( 'NONE',  ( -19.19277407259999180, 26.35772955756921121, -2.500000000000000000 ) ) ;
#6059=ORIENTED_EDGE ( 'NONE', *, *, #8008, .T. ) ;
#6113=VERTEX_POINT ( 'NONE', #6220 ) ;
#6217=ORIENTED_EDGE ( 'NONE', *, *, #7210, .T. ) ;
#6220=CARTESIAN_POINT ( 'NONE',  ( -9.489957111606940998, 28.27083100358139944, 2.500000000000000000 ) ) ;
#6236=CIRCLE ( 'NONE', #2053, 3.499999999999996891 ) ;
#6346=AXIS2_PLACEMENT_3D ( 'NONE', #18822, #10266, #22478 ) ;
#6562=DIRECTION ( 'NONE',  ( 0.000000000000000000, -1.000000000000000000, 1.011971878839179923E-16 ) ) ;
#6594=FACE_BOUND ( 'NONE', #20717, .T. ) ;
#6654=EDGE_CURVE ( 'NONE', #19958, #22663, #19485, .T. ) ;
#6677=CARTESIAN_POINT ( 'NONE',  ( -18.05391955182270181, 22.49081825942809942, -2.500000000000000000 ) ) ;
#6683=FACE_OUTER_BOUND ( 'NONE', #4188, .T. ) ;
#6785=EDGE_CURVE ( 'NONE', #18892, #19958, #21242, .T. ) ;
#6840=PRODUCT_DEFINITION ( 'UNKNOWN', '', #796, #9424 ) ;
#6879=CARTESIAN_POINT ( 'NONE',  ( -1.276518118481687392, 16.16736622398676460, -1.549884229762907576E-17 ) ) ;
#6888=ORIENTED_EDGE ( 'NONE', *, *, #1340, .F. ) ;
#6948=DIRECTION ( 'NONE',  ( 0.9730401042858036753, -0.2306359803922028995, 2.740969466505749537E-16 ) ) ;
#6953=DIRECTION ( 'NONE',  ( -0.9730401042858033422, 0.2306359803922031215, -1.141364251305443211E-16 ) ) ;
#6969=DIRECTION ( 'NONE',  ( -0.9730401042858035643, 0.2306359803922028717, -2.740969466505749044E-16 ) ) ;
#7041=CARTESIAN_POINT ( 'NONE',  ( -12.99532053203719961, 13.48190178978399878, 2.500000000000000000 ) ) ;
#7064=VERTEX_POINT ( 'NONE', #16590 ) ;
#7085=VECTOR ( 'NONE', #6948, 999.9999999999998863 ) ;
#7090=ORIENTED_EDGE ( 'NONE', *, *, #7454, .T. ) ;
#7097=EDGE_LOOP ( 'NONE', ( #19792, #1868, #2403 ) ) ;
#7110=LINE ( 'NONE', #19800, #14553 ) ;
#7210=EDGE_CURVE ( 'NONE', #4832, #851, #10069, .T. ) ;
#7263=ORIENTED_EDGE ( 'NONE', *, *, #3233, .T. ) ;
#7331=EDGE_CURVE ( 'NONE', #12726, #851, #7336, .T. ) ;
#7336=CIRCLE ( 'NONE', #2411, 7.999999999999998224 ) ;
#7454=EDGE_CURVE ( 'NONE', #5237, #11903, #15969, .T. ) ;
#7513=AXIS2_PLACEMENT_3D ( 'NONE', #7776, #8248, #1333 ) ;
#7521=DIRECTION ( 'NONE',  ( 0.9730401042858033422, -0.2306359803922031215, 3.994774879569051239E-16 ) ) ;
#7523=ORIENTED_EDGE ( 'NONE', *, *, #6654, .T. ) ;
#7563=ORIENTED_EDGE ( 'NONE', *, *, #3881, .F. ) ;
#7613=EDGE_CURVE ( 'NONE', #11939, #2591, #11239, .T. ) ;
#7620=ORIENTED_EDGE ( 'NONE', *, *, #7210, .F. ) ;
#7640=DIRECTION ( 'NONE',  ( 0.2306359803922025387, 0.9730401042858035643, -4.741332172907917461E-18 ) ) ;
#7725=FACE_OUTER_BOUND ( 'NONE', #14107, .T. ) ;
#7776=CARTESIAN_POINT ( 'NONE',  ( -12.33340651292470014, 21.13490689743859718, -3.289309883929029635E-15 ) ) ;
#7799=DIRECTION ( 'NONE',  ( 0.9730401042858035643, -0.2306359803922028717, 2.740969466505749044E-16 ) ) ;
#7844=EDGE_LOOP ( 'NONE', ( #14186, #20921, #17534, #19071 ) ) ;
#7848=DIRECTION ( 'NONE',  ( 0.2306359803922031215, 0.9730401042858034533, -4.741332172907939802E-18 ) ) ;
#7857=DIRECTION ( 'NONE',  ( -0.9730401042858036753, 0.2306359803922028995, -2.740969466505749537E-16 ) ) ;
#7897=CARTESIAN_POINT ( 'NONE',  ( -12.09504422718935857, 22.14054384521797303, -3.294210050729730189E-15 ) ) ;
#7925=FACE_OUTER_BOUND ( 'NONE', #11448, .T. ) ;
#7971=VECTOR ( 'NONE', #11828, 999.9999999999998863 ) ;
#7987=ORIENTED_EDGE ( 'NONE', *, *, #8545, .F. ) ;
#8008=EDGE_CURVE ( 'NONE', #587, #5237, #2120, .T. ) ;
#8063=CIRCLE ( 'NONE', #5412, 7.999999999999997335 ) ;
#8144=DIRECTION ( 'NONE',  ( -0.9730401042858036753, 0.2306359803922024831, 0.000000000000000000 ) ) ;
#8219=ORIENTED_EDGE ( 'NONE', *, *, #20431, .F. ) ;
#8248=DIRECTION ( 'NONE',  ( 0.9730401042858035643, -0.2306359803922028717, 2.740969466505749044E-16 ) ) ;
#8281=AXIS2_PLACEMENT_3D ( 'NONE', #484, #18797, #9771 ) ;
#8458=AXIS2_PLACEMENT_3D ( 'NONE', #16555, #23454, #283 ) ;
#8545=EDGE_CURVE ( 'NONE', #238, #19010, #7110, .T. ) ;
#8718=CARTESIAN_POINT ( 'NONE',  ( -18.05391955182270181, 22.49081825942809942, -2.500000000000000000 ) ) ;
#8724=ORIENTED_EDGE ( 'NONE', *, *, #7613, .F. ) ;
#8742=CARTESIAN_POINT ( 'NONE',  ( -18.05391955182270181, 22.49081825942809942, -4.900728725074969882E-15 ) ) ;
#8764=AXIS2_PLACEMENT_3D ( 'NONE', #6677, #17467, #21256 ) ;
#8773=LINE ( 'NONE', #6879, #2543 ) ;
#8817=AXIS2_PLACEMENT_3D ( 'NONE', #11643, #13404, #2701 ) ;
#8949=CARTESIAN_POINT ( 'NONE',  ( 1.213484035536889882, 25.73383521926719908, 2.500000000000000000 ) ) ;
#8979=DIRECTION ( 'NONE',  ( 0.2306359803922028995, 0.9730401042858035643, -4.741332172907957521E-18 ) ) ;
#9052=CONICAL_SURFACE ( 'NONE', #2560, 1.033499999999998753, 1.029744258676650093 ) ;
#9060=EDGE_CURVE ( 'NONE', #22465, #22663, #22490, .T. ) ;
#9085=EDGE_CURVE ( 'NONE', #11939, #1307, #5459, .T. ) ;
#9174=ORIENTED_EDGE ( 'NONE', *, *, #2005, .T. ) ;
#9200=DIRECTION ( 'NONE',  ( -0.9730401042858036753, 0.2306359803922031493, -2.740969466505752002E-16 ) ) ;
#9212=CARTESIAN_POINT ( 'NONE',  ( -0.5391976746782148888, 18.33937061236850141, 3.301631463538509622E-17 ) ) ;
#9240=DIRECTION ( 'NONE',  ( 0.9730401042858035643, -0.2306359803922028717, 2.740969466505749044E-16 ) ) ;
#9297=DIRECTION ( 'NONE',  ( 0.9730401042858035643, -0.2306359803922024276, 0.000000000000000000 ) ) ;
#9335=EDGE_LOOP ( 'NONE', ( #754, #11018, #21019, #2168, #15781, #5202, #18093, #6217, #4031 ) ) ;
#9370=AXIS2_PLACEMENT_3D ( 'NONE', #19522, #3245, #23182 ) ;
#9376=CARTESIAN_POINT ( 'NONE',  ( -12.57176879866004349, 20.12926994965922134, -3.157842470436450709E-15 ) ) ;
#9388=DIRECTION ( 'NONE',  ( 0.2306359803922033713, 0.9730401042858035643, -4.741332172907925165E-18 ) ) ;
#9407=CONICAL_SURFACE ( 'NONE', #18906, 2.283500000000000529, 0.7853981633974476129 ) ;
#9424=DESIGN_CONTEXT ( 'detailed design', #4269, 'design' ) ;
#9463=ORIENTED_EDGE ( 'NONE', *, *, #11639, .T. ) ;
#9726=DIRECTION ( 'NONE',  ( -0.2306359803922028995, -0.9730401042858034533, 4.741332172907957521E-18 ) ) ;
#9771=DIRECTION ( 'NONE',  ( 0.2306359803922031215, 0.9730401042858034533, -4.741332172907939802E-18 ) ) ;
#9778=AXIS2_PLACEMENT_3D ( 'NONE', #13042, #5435, #10922 ) ;
#9808=CIRCLE ( 'NONE', #15859, 7.999999999999998224 ) ;
#9826=EDGE_CURVE ( 'NONE', #22663, #21240, #13308, .T. ) ;
#9964=CIRCLE ( 'NONE', #3500, 7.999999999999997335 ) ;
#10004=ORIENTED_EDGE ( 'NONE', *, *, #19682, .T. ) ;
#10017=VECTOR ( 'NONE', #17839, 1000.000000000000114 ) ;
#10069=LINE ( 'NONE', #13607, #16794 ) ;
#10092=SHAPE_REPRESENTATION ( '1602p_c_33', ( #12739 ), #20868 ) ;
#10133=CARTESIAN_POINT ( 'NONE',  ( -5.303405830673253440, 11.24695771925867760, -1.731061307250961080E-15 ) ) ;
#10135=CARTESIAN_POINT ( 'NONE',  ( -26.17677262429019791, 24.41614710630589968, 2.500000000000000000 ) ) ;
#10165=CIRCLE ( 'NONE', #1400, 7.999999999999997335 ) ;
#10216=DIRECTION ( 'NONE',  ( 0.5249589903860232276, -0.8511275218278909760, 1.971684378104701054E-16 ) ) ;
#10251=FACE_BOUND ( 'NONE', #13484, .T. ) ;
#10266=DIRECTION ( 'NONE',  ( 4.063875459488295522E-16, -1.011971878839177951E-16, -1.000000000000000000 ) ) ;
#10269=AXIS2_PLACEMENT_3D ( 'NONE', #17961, #21608, #19609 ) ;
#10287=DIRECTION ( 'NONE',  ( 0.2306359803922031215, 0.9730401042858034533, -4.741332172907939802E-18 ) ) ;
#10306=ORIENTED_EDGE ( 'NONE', *, *, #10691, .T. ) ;
#10322=ADVANCED_FACE ( 'NONE', ( #19201 ), #17771, .T. ) ;
#10492=ADVANCED_FACE ( 'NONE', ( #3735 ), #18235, .T. ) ;
#10535=CARTESIAN_POINT ( 'NONE',  ( -0.2232035960304966093, 20.61124038026003191, -3.168006029165981644E-16 ) ) ;
#10541=ORIENTED_EDGE ( 'NONE', *, *, #10691, .F. ) ;
#10544=DIRECTION ( 'NONE',  ( -2.656137997592320068E-16, 6.783012436524469908E-17, 1.000000000000000000 ) ) ;
#10569=CIRCLE ( 'NONE', #20784, 2.067000000000000615 ) ;
#10626=CARTESIAN_POINT ( 'NONE',  ( -3.458317987535628912, 19.03127855354509990, -5.000000000000000888 ) ) ;
#10636=CARTESIAN_POINT ( 'NONE',  ( -11.24263882182209962, 20.87636639668270178, -2.982050098520939832E-15 ) ) ;
#10659=DIRECTION ( 'NONE',  ( -0.2306359803922027885, -0.9730401042858034533, 4.741332172908048425E-18 ) ) ;
#10691=EDGE_CURVE ( 'NONE', #4833, #7064, #20363, .T. ) ;
#10728=VERTEX_POINT ( 'NONE', #4446 ) ;
#10748=CIRCLE ( 'NONE', #11118, 2.500000000000000000 ) ;
#10775=CARTESIAN_POINT ( 'NONE',  ( -6.610902845792273830, 17.65425360406484856, -1.280106301620261415E-15 ) ) ;
#10847=ADVANCED_FACE ( 'NONE', ( #6594, #1335 ), #985, .F. ) ;
#10865=CIRCLE ( 'NONE', #19200, 2.066999999999997062 ) ;
#10880=CARTESIAN_POINT ( 'NONE',  ( -11.72915887396500167, 20.99168438687879856, -3.119098571846229552E-15 ) ) ;
#10922=DIRECTION ( 'NONE',  ( -1.918983243708115015E-32, 3.790318773197884981E-16, -1.000000000000000000 ) ) ;
#10928=DIRECTION ( 'NONE',  ( -0.9730401042858036753, 0.2306359803922031493, -2.740969466505752002E-16 ) ) ;
#10974=EDGE_CURVE ( 'NONE', #22662, #5508, #16556, .T. ) ;
#10987=ORIENTED_EDGE ( 'NONE', *, *, #2871, .F. ) ;
#11018=ORIENTED_EDGE ( 'NONE', *, *, #4849, .F. ) ;
#11118=AXIS2_PLACEMENT_3D ( 'NONE', #18605, #13715, #20957 ) ;
#11179=CARTESIAN_POINT ( 'NONE',  ( -11.24263882182209962, 20.87636639668270178, -2.500000000000000000 ) ) ;
#11218=ORIENTED_EDGE ( 'NONE', *, *, #3881, .T. ) ;
#11239=LINE ( 'NONE', #18466, #14547 ) ;
#11250=CARTESIAN_POINT ( 'NONE',  ( -0.5391976746782148888, 18.33937061236850141, 3.301631463538509622E-17 ) ) ;
#11305=CIRCLE ( 'NONE', #6346, 7.599342076785325695 ) ;
#11309=CARTESIAN_POINT ( 'NONE',  ( -18.05391955182270181, 22.49081825942809942, -4.900728725074969882E-15 ) ) ;
#11331=AXIS2_PLACEMENT_3D ( 'NONE', #2546, #4207, #18590 ) ;
#11371=EDGE_LOOP ( 'NONE', ( #17591, #9174 ) ) ;
#11373=VERTEX_POINT ( 'NONE', #10133 ) ;
#11448=EDGE_LOOP ( 'NONE', ( #14969, #2274, #7263, #20283 ) ) ;
#11605=DIRECTION ( 'NONE',  ( -0.9730401042858035643, 0.2306359803922031215, -2.740969466505752002E-16 ) ) ;
#11639=EDGE_CURVE ( 'NONE', #5508, #19958, #9808, .T. ) ;
#11643=CARTESIAN_POINT ( 'NONE',  ( -20.00000000397270128, 22.95208919256889857, -5.448922613368719782E-15 ) ) ;
#11647=VECTOR ( 'NONE', #21481, 1000.000000000000114 ) ;
#11828=DIRECTION ( 'NONE',  ( 0.9730401042858036753, -0.2306359803922028995, 2.740969466505749537E-16 ) ) ;
#11898=ADVANCED_FACE ( 'NONE', ( #417 ), #9407, .F. ) ;
#11903=VERTEX_POINT ( 'NONE', #20274 ) ;
#11910=ORIENTED_EDGE ( 'NONE', *, *, #4288, .F. ) ;
#11933=FACE_OUTER_BOUND ( 'NONE', #22268, .T. ) ;
#11939=VERTEX_POINT ( 'NONE', #6011 ) ;
#12025=CIRCLE ( 'NONE', #14284, 3.000000000000000444 ) ;
#12127=EDGE_CURVE ( 'NONE', #16276, #2591, #19658, .T. ) ;
#12130=DIRECTION ( 'NONE',  ( -0.9730401042858036753, 0.2306359803922028995, -2.740969466505749537E-16 ) ) ;
#12134=CARTESIAN_POINT ( 'NONE',  ( -11.24263882182209962, 20.87636639668270178, 2.500000000000000000 ) ) ;
#12186=CARTESIAN_POINT ( 'NONE',  ( -12.99532053203719961, 13.48190178978399878, -2.500000000000000000 ) ) ;
#12215=ORIENTED_EDGE ( 'NONE', *, *, #1179, .T. ) ;
#12277=EDGE_CURVE ( 'NONE', #7064, #15418, #3030, .T. ) ;
#12296=SHAPE_DEFINITION_REPRESENTATION ( #18025, #10092 ) ;
#12336=EDGE_CURVE ( 'NONE', #4833, #5237, #10569, .T. ) ;
#12364=ORIENTED_EDGE ( 'NONE', *, *, #18742, .T. ) ;
#12431=ORIENTED_EDGE ( 'NONE', *, *, #12277, .T. ) ;
#12445=EDGE_LOOP ( 'NONE', ( #4631, #4162, #2502, #9463, #7523 ) ) ;
#12467=AXIS2_PLACEMENT_3D ( 'NONE', #17657, #19086, #17299 ) ;
#12570=CARTESIAN_POINT ( 'NONE',  ( -12.33340651292470014, 21.13490689743859718, -3.289309883929029635E-15 ) ) ;
#12573=ORIENTED_EDGE ( 'NONE', *, *, #6785, .F. ) ;
#12622=CIRCLE ( 'NONE', #17549, 2.500000000000000000 ) ;
#12661=CARTESIAN_POINT ( 'NONE',  ( -0.5391976746782148888, 18.33937061236850141, 3.301631463538509622E-17 ) ) ;
#12726=VERTEX_POINT ( 'NONE', #14172 ) ;
#12739=AXIS2_PLACEMENT_3D ( 'NONE', #2569, #13380, #415 ) ;
#12795=AXIS2_PLACEMENT_3D ( 'NONE', #5609, #23304, #7521 ) ;
#12830=DIRECTION ( 'NONE',  ( 2.086281924601080239E-16, 1.946516371809877606E-18, -1.000000000000000000 ) ) ;
#12853=LINE ( 'NONE', #8949, #7085 ) ;
#12896=EDGE_LOOP ( 'NONE', ( #606, #13489, #2192, #23070, #15731 ) ) ;
#12897=EDGE_CURVE ( 'NONE', #11373, #12726, #16516, .T. ) ;
#12968=ORIENTED_EDGE ( 'NONE', *, *, #3956, .F. ) ;
#12981=UNCERTAINTY_MEASURE_WITH_UNIT (LENGTH_MEASURE( 1.000000000000000082E-05 ), #2012, 'distance_accuracy_value', 'NONE');
#13009=EDGE_CURVE ( 'NONE', #19010, #22465, #18525, .T. ) ;
#13023=PLANE ( 'NONE',  #8458 ) ;
#13038=ORIENTED_EDGE ( 'NONE', *, *, #18074, .T. ) ;
#13042=CARTESIAN_POINT ( 'NONE',  ( -11.24263882182209962, 20.87636639668270178, -8.642052169251309479 ) ) ;
#13116=CARTESIAN_POINT ( 'NONE',  ( -18.05391955182270181, 22.49081825942809942, -4.900728725074969882E-15 ) ) ;
#13298=ADVANCED_FACE ( 'NONE', ( #1627 ), #21573, .F. ) ;
#13308=CIRCLE ( 'NONE', #8764, 7.599342076785325695 ) ;
#13311=EDGE_LOOP ( 'NONE', ( #21572, #10004 ) ) ;
#13326=ADVANCED_FACE ( 'NONE', ( #16571 ), #9052, .F. ) ;
#13374=VECTOR ( 'NONE', #18836, 1000.000000000000000 ) ;
#13380=DIRECTION ( 'NONE',  ( 0.000000000000000000, 0.000000000000000000, 1.000000000000000000 ) ) ;
#13404=DIRECTION ( 'NONE',  ( -2.656137997592320068E-16, 6.783012436524469908E-17, 1.000000000000000000 ) ) ;
#13480=CARTESIAN_POINT ( 'NONE',  ( -3.458317987535630689, 19.03127855354509990, 4.999999999999999112 ) ) ;
#13484=EDGE_LOOP ( 'NONE', ( #2252, #13038 ) ) ;
#13489=ORIENTED_EDGE ( 'NONE', *, *, #4849, .T. ) ;
#13512=FACE_OUTER_BOUND ( 'NONE', #14841, .T. ) ;
#13589=LINE ( 'NONE', #20038, #14499 ) ;
#13607=CARTESIAN_POINT ( 'NONE',  ( -2.291879384893320104, 10.94490600546980019, 2.500000000000000000 ) ) ;
#13629=CARTESIAN_POINT ( 'NONE',  ( -16.20883170868506085, 30.27513909371458567, -4.938659382458227626E-15 ) ) ;
#13715=DIRECTION ( 'NONE',  ( 0.9730401042858036753, -0.2306359803922031493, 2.740969466505752002E-16 ) ) ;
#13807=DIRECTION ( 'NONE',  ( 4.063875459488300452E-16, -1.011971878839179923E-16, -1.000000000000000000 ) ) ;
#14014=EDGE_CURVE ( 'NONE', #19785, #10728, #14338, .T. ) ;
#14069=CYLINDRICAL_SURFACE ( 'NONE', #17741, 2.066999999999997062 ) ;
#14087=ORIENTED_EDGE ( 'NONE', *, *, #9826, .F. ) ;
#14107=EDGE_LOOP ( 'NONE', ( #23020, #22506, #10306, #597 ) ) ;
#14109=CIRCLE ( 'NONE', #3867, 2.999999999999999556 ) ;
#14127=CARTESIAN_POINT ( 'NONE',  ( 1.305890168459409084, 26.12369144665493437, -4.914342747878582431E-18 ) ) ;
#14130=ADVANCED_FACE ( 'NONE', ( #4091 ), #17757, .F. ) ;
#14169=AXIS2_PLACEMENT_3D ( 'NONE', #10880, #21880, #7640 ) ;
#14172=CARTESIAN_POINT ( 'NONE',  ( -19.89900739496031434, 14.70649742514172331, -5.842515507009584646E-15 ) ) ;
#14186=ORIENTED_EDGE ( 'NONE', *, *, #9085, .F. ) ;
#14284=AXIS2_PLACEMENT_3D ( 'NONE', #10626, #17854, #9297 ) ;
#14303=DIRECTION ( 'NONE',  ( 0.2306359803922031215, 0.9730401042858034533, -4.741332172907939802E-18 ) ) ;
#14338=CIRCLE ( 'NONE', #11331, 4.999999999999997335 ) ;
#14497=ORIENTED_EDGE ( 'NONE', *, *, #18074, .F. ) ;
#14499=VECTOR ( 'NONE', #4006, 1000.000000000000000 ) ;
#14547=VECTOR ( 'NONE', #2180, 1000.000000000000000 ) ;
#14550=DIRECTION ( 'NONE',  ( 0.8511275218278916421, 0.5249589903860222284, 1.038675759242784740E-16 ) ) ;
#14553=VECTOR ( 'NONE', #16236, 1000.000000000000114 ) ;
#14573=AXIS2_PLACEMENT_3D ( 'NONE', #5827, #457, #12830 ) ;
#14665=DIRECTION ( 'NONE',  ( 0.2306359803922031215, 0.9730401042858033422, -4.741332172907962143E-18 ) ) ;
#14668=CARTESIAN_POINT ( 'NONE',  ( -3.458317987535629801, 19.03127855354509990, -7.892745253163399067E-16 ) ) ;
#14818=LINE ( 'NONE', #11179, #10017 ) ;
#14828=DIRECTION ( 'NONE',  ( 0.3034590813640733464, -0.9528444710117558447, 2.502071977558823078E-16 ) ) ;
#14841=EDGE_LOOP ( 'NONE', ( #8724, #4984, #22554, #14497 ) ) ;
#14884=CARTESIAN_POINT ( 'NONE',  ( -20.80722593534541076, 19.54644882756858948, -2.500000000000000000 ) ) ;
#14905=DIRECTION ( 'NONE',  ( 0.2306359803922028717, 0.9730401042858035643, -7.445392196378163890E-17 ) ) ;
#14969=ORIENTED_EDGE ( 'NONE', *, *, #12277, .F. ) ;
#15080=CARTESIAN_POINT ( 'NONE',  ( -1.115787625658725135, 15.90677035165398046, 4.486964506765413337E-17 ) ) ;
#15084=ORIENTED_EDGE ( 'NONE', *, *, #2845, .F. ) ;
#15131=CARTESIAN_POINT ( 'NONE',  ( -1.613230144398002386, 26.81559938783153996, -8.272051826996034682E-16 ) ) ;
#15343=CARTESIAN_POINT ( 'NONE',  ( -18.05391955182270181, 22.49081825942809942, -4.900728725074969882E-15 ) ) ;
#15418=VERTEX_POINT ( 'NONE', #16006 ) ;
#15430=ORIENTED_EDGE ( 'NONE', *, *, #10974, .F. ) ;
#15458=ORIENTED_EDGE ( 'NONE', *, *, #1340, .T. ) ;
#15522=DIRECTION ( 'NONE',  ( -1.000000000000000000, 0.000000000000000000, 0.000000000000000000 ) ) ;
#15613=ORIENTED_EDGE ( 'NONE', *, *, #8545, .T. ) ;
#15631=EDGE_CURVE ( 'NONE', #1307, #16276, #13589, .T. ) ;
#15672=FACE_OUTER_BOUND ( 'NONE', #12896, .T. ) ;
#15701=FACE_BOUND ( 'NONE', #22907, .T. ) ;
#15731=ORIENTED_EDGE ( 'NONE', *, *, #14014, .T. ) ;
#15781=ORIENTED_EDGE ( 'NONE', *, *, #11639, .F. ) ;
#15859=AXIS2_PLACEMENT_3D ( 'NONE', #11309, #2242, #22191 ) ;
#15867=CARTESIAN_POINT ( 'NONE',  ( -20.00000000397270128, 22.95208919256889857, -5.448922613368719782E-15 ) ) ;
#15907=CARTESIAN_POINT ( 'NONE',  ( -0.9605240398339689456, 18.43923599187829865, -8.566766326431390468E-17 ) ) ;
#15969=LINE ( 'NONE', #10775, #19463 ) ;
#15978=DIRECTION ( 'NONE',  ( 1.000000000000000000, 0.000000000000000000, 0.000000000000000000 ) ) ;
#15992=CARTESIAN_POINT ( 'NONE',  ( -20.00000000397270128, 22.95208919256889857, -2.500000000000000000 ) ) ;
#16006=CARTESIAN_POINT ( 'NONE',  ( 0.03739227630228923044, 20.77197087308299572, -2.849987155837237711E-16 ) ) ;
#16011=CARTESIAN_POINT ( 'NONE',  ( -20.00000000397270128, 22.95208919256889857, 2.500000000000000000 ) ) ;
#16090=CYLINDRICAL_SURFACE ( 'NONE', #4828, 8.000000000000003553 ) ;
#16122=DIRECTION ( 'NONE',  ( 0.2306359803922037599, 0.9730401042858033422, -4.741332172908110825E-18 ) ) ;
#16236=DIRECTION ( 'NONE',  ( 0.9730401042858035643, -0.2306359803922031215, 2.740969466505752002E-16 ) ) ;
#16276=VERTEX_POINT ( 'NONE', #20914 ) ;
#16316=DIRECTION ( 'NONE',  ( 0.2306359803922025387, 0.9730401042858035643, -4.741332172907917461E-18 ) ) ;
#16333=ADVANCED_FACE ( 'NONE', ( #11933 ), #17257, .T. ) ;
#16344=ADVANCED_FACE ( 'NONE', ( #10251, #6683 ), #19374, .F. ) ;
#16427=ADVANCED_BREP_SHAPE_REPRESENTATION ( '', ( #17699, #12739 ), #20868 ) ;
#16516=LINE ( 'NONE', #599, #20032 ) ;
#16555=CARTESIAN_POINT ( 'NONE',  ( -11.24263882182209962, 20.87636639668270178, 2.500000000000000000 ) ) ;
#16556=CIRCLE ( 'NONE', #12795, 7.599342076785325695 ) ;
#16565=ADVANCED_FACE ( 'NONE', ( #7725 ), #333, .F. ) ;
#16571=FACE_OUTER_BOUND ( 'NONE', #7097, .T. ) ;
#16590=CARTESIAN_POINT ( 'NONE',  ( -0.4837994683632851900, 20.45050988743705744, -3.168006029165976713E-16 ) ) ;
#16606=VERTEX_POINT ( 'NONE', #20311 ) ;
#16624=CLOSED_SHELL ( 'NONE', ( #22316, #17656, #10322, #3694, #14130, #22354, #11898, #21672, #16565, #17343, #13326, #19880, #16344, #18730, #10847, #13298, #16333, #17922, #10492 ) ) ;
#16664=CARTESIAN_POINT ( 'NONE',  ( -0.5391976746782148888, 18.33937061236850141, 3.301631463538509622E-17 ) ) ;
#16794=VECTOR ( 'NONE', #23082, 999.9999999999998863 ) ;
#17001=ORIENTED_EDGE ( 'NONE', *, *, #20735, .T. ) ;
#17064=DIRECTION ( 'NONE',  ( 1.224646799147353207E-16, 1.000000000000000000, -0.000000000000000000 ) ) ;
#17235=CARTESIAN_POINT ( 'NONE',  ( -12.20588344543568837, 18.98041049132002556, -2.856163744861079589E-15 ) ) ;
#17240=VERTEX_POINT ( 'NONE', #1190 ) ;
#17257=SPHERICAL_SURFACE ( 'NONE', #20566, 8.000000000000000000 ) ;
#17288=ORIENTED_EDGE ( 'NONE', *, *, #19946, .F. ) ;
#17299=DIRECTION ( 'NONE',  ( -0.2306359803922030105, -0.9730401042858034533, 0.000000000000000000 ) ) ;
#17343=ADVANCED_FACE ( 'NONE', ( #5879, #15701 ), #17472, .T. ) ;
#17368=DIRECTION ( 'NONE',  ( 0.000000000000000000, 1.000000000000000000, 0.000000000000000000 ) ) ;
#17423=FACE_OUTER_BOUND ( 'NONE', #7844, .T. ) ;
#17448=EDGE_LOOP ( 'NONE', ( #2101, #7090, #22695, #10541 ) ) ;
#17459=DIRECTION ( 'NONE',  ( -0.9730401042858036753, 0.2306359803922031493, -2.740969466505752002E-16 ) ) ;
#17467=DIRECTION ( 'NONE',  ( -1.248400535696349791E-16, 3.446306084657139973E-17, 1.000000000000000000 ) ) ;
#17472=PLANE ( 'NONE',  #2423 ) ;
#17534=ORIENTED_EDGE ( 'NONE', *, *, #12127, .F. ) ;
#17549=AXIS2_PLACEMENT_3D ( 'NONE', #9212, #20258, #20015 ) ;
#17578=CARTESIAN_POINT ( 'NONE',  ( -3.458317987535629801, 19.03127855354509990, -7.892745253163399067E-16 ) ) ;
#17591=ORIENTED_EDGE ( 'NONE', *, *, #5759, .F. ) ;
#17656=ADVANCED_FACE ( 'NONE', ( #21841 ), #19489, .T. ) ;
#17657=CARTESIAN_POINT ( 'NONE',  ( -20.00000000397270128, 22.95208919256889857, 2.500000000000000000 ) ) ;
#17658=SHAPE_REPRESENTATION_RELATIONSHIP ( 'NONE' , 'NONE' ,  #10092, #16427 ) ;
#17699=MANIFOLD_SOLID_BREP ( 'Imported1', #16624 ) ;
#17741=AXIS2_PLACEMENT_3D ( 'NONE', #21313, #21433, #19767 ) ;
#17757=CONICAL_SURFACE ( 'NONE', #7513, 1.033499999999998753, 1.029744258676650093 ) ;
#17771=SPHERICAL_SURFACE ( 'NONE', #19395, 8.000000000000000000 ) ;
#17795=ORIENTED_EDGE ( 'NONE', *, *, #7331, .T. ) ;
#17810=ORIENTED_EDGE ( 'NONE', *, *, #4288, .T. ) ;
#17839=DIRECTION ( 'NONE',  ( 0.2306359803922031215, 0.9730401042858035643, -4.741332172907962143E-18 ) ) ;
#17854=DIRECTION ( 'NONE',  ( -0.2306359803922028717, -0.9730401042858035643, -4.801075795095373112E-17 ) ) ;
#17922=ADVANCED_FACE ( 'NONE', ( #15672 ), #1286, .T. ) ;
#17940=AXIS2_PLACEMENT_3D ( 'NONE', #8718, #20946, #6953 ) ;
#17961=CARTESIAN_POINT ( 'NONE',  ( -3.458317987535629801, 19.03127855354509990, -7.892745253163399067E-16 ) ) ;
#18001=FACE_OUTER_BOUND ( 'NONE', #23343, .T. ) ;
#18005=CARTESIAN_POINT ( 'NONE',  ( -11.72915887396500167, 20.99168438687879856, -3.119098571846229552E-15 ) ) ;
#18025=PRODUCT_DEFINITION_SHAPE ( 'NONE', 'NONE',  #6840 ) ;
#18074=EDGE_CURVE ( 'NONE', #2591, #16276, #6236, .T. ) ;
#18090=AXIS2_PLACEMENT_3D ( 'NONE', #22166, #10928, #190 ) ;
#18093=ORIENTED_EDGE ( 'NONE', *, *, #5759, .T. ) ;
#18120=CARTESIAN_POINT ( 'NONE',  ( -0.5391976746782148888, 18.33937061236850141, 3.301631463538509622E-17 ) ) ;
#18235=CYLINDRICAL_SURFACE ( 'NONE', #791, 8.000000000000003553 ) ;
#18466=CARTESIAN_POINT ( 'NONE',  ( -19.19277407259999180, 26.35772955756921121, -5.465517275973897116E-15 ) ) ;
#18481=DIRECTION ( 'NONE',  ( 0.2306359803922030938, 0.9730401042858035643, -4.741332172907964454E-18 ) ) ;
#18525=CIRCLE ( 'NONE', #8281, 7.999999999999998224 ) ;
#18590=DIRECTION ( 'NONE',  ( 0.2306359803922031215, 0.9730401042858033422, -4.741332172907962143E-18 ) ) ;
#18592=CARTESIAN_POINT ( 'NONE',  ( -19.19277407259999180, 26.35772955756921121, 2.500000000000000000 ) ) ;
#18596=DIRECTION ( 'NONE',  ( 3.837966487416234409E-32, -1.188439662295820021E-15, -1.000000000000000000 ) ) ;
#18603=ORIENTED_EDGE ( 'NONE', *, *, #19682, .F. ) ;
#18605=CARTESIAN_POINT ( 'NONE',  ( -0.5391976746782148888, 18.33937061236850141, 3.301631463538509622E-17 ) ) ;
#18730=ADVANCED_FACE ( 'NONE', ( #21793 ), #13023, .F. ) ;
#18742=EDGE_CURVE ( 'NONE', #18892, #17240, #8063, .T. ) ;
#18797=DIRECTION ( 'NONE',  ( 0.9730401042858036753, -0.2306359803922031493, -8.741838862554654777E-17 ) ) ;
#18822=CARTESIAN_POINT ( 'NONE',  ( -18.05391955182270181, 22.49081825942809942, 2.500000000000000000 ) ) ;
#18836=DIRECTION ( 'NONE',  ( 0.6988463228792121118, 0.7152718483193672983, 1.371062488412534409E-16 ) ) ;
#18865=AXIS2_PLACEMENT_3D ( 'NONE', #4478, #904, #9726 ) ;
#18892=VERTEX_POINT ( 'NONE', #15131 ) ;
#18906=AXIS2_PLACEMENT_3D ( 'NONE', #5779, #7799, #22517 ) ;
#18994=ORIENTED_EDGE ( 'NONE', *, *, #3873, .T. ) ;
#19010=VERTEX_POINT ( 'NONE', #12186 ) ;
#19039=EDGE_LOOP ( 'NONE', ( #22371, #7563 ) ) ;
#19071=ORIENTED_EDGE ( 'NONE', *, *, #15631, .F. ) ;
#19086=DIRECTION ( 'NONE',  ( 4.063875459488300452E-16, -1.011971878839181895E-16, -1.000000000000000000 ) ) ;
#19089=AXIS2_PLACEMENT_3D ( 'NONE', #583, #2129, #9388 ) ;
#19200=AXIS2_PLACEMENT_3D ( 'NONE', #15907, #17459, #23133 ) ;
#19201=FACE_OUTER_BOUND ( 'NONE', #12445, .T. ) ;
#19297=DIRECTION ( 'NONE',  ( 0.9730401042858036753, -0.2306359803922031493, 6.356122819266963936E-16 ) ) ;
#19374=PLANE ( 'NONE',  #21330 ) ;
#19395=AXIS2_PLACEMENT_3D ( 'NONE', #8742, #21200, #15978 ) ;
#19463=VECTOR ( 'NONE', #21781, 999.9999999999998863 ) ;
#19472=EDGE_LOOP ( 'NONE', ( #20095, #18603, #7987, #11910, #14087 ) ) ;
#19485=CIRCLE ( 'NONE', #2748, 7.999999999999998224 ) ;
#19489=TOROIDAL_SURFACE ( 'NONE', #14573, 5.000000000000000000, 3.000000000000000000 ) ;
#19522=CARTESIAN_POINT ( 'NONE',  ( -11.24263882182209962, 20.87636639668270178, -2.500000000000000000 ) ) ;
#19586=ORIENTED_EDGE ( 'NONE', *, *, #1319, .F. ) ;
#19602=ORIENTED_EDGE ( 'NONE', *, *, #3617, .F. ) ;
#19609=DIRECTION ( 'NONE',  ( 0.2306359803922030938, 0.9730401042858035643, -4.741332172907964454E-18 ) ) ;
#19658=CIRCLE ( 'NONE', #12467, 3.499999999999996891 ) ;
#19682=EDGE_CURVE ( 'NONE', #19010, #22465, #14818, .T. ) ;
#19767=DIRECTION ( 'NONE',  ( 0.2306359803922033713, 0.9730401042858035643, -4.741332172907925165E-18 ) ) ;
#19785=VERTEX_POINT ( 'NONE', #436 ) ;
#19792=ORIENTED_EDGE ( 'NONE', *, *, #8008, .F. ) ;
#19800=CARTESIAN_POINT ( 'NONE',  ( -2.291879384893320104, 10.94490600546980019, -2.500000000000000000 ) ) ;
#19880=ADVANCED_FACE ( 'NONE', ( #13512 ), #914, .F. ) ;
#19903=DIRECTION ( 'NONE',  ( -0.9730401042858035643, 0.2306359803922028717, -2.740969466505749044E-16 ) ) ;
#19946=EDGE_CURVE ( 'NONE', #21240, #22662, #5031, .T. ) ;
#19958=VERTEX_POINT ( 'NONE', #13629 ) ;
#19999=CARTESIAN_POINT ( 'NONE',  ( -9.489957111606940998, 28.27083100358139944, -2.500000000000000000 ) ) ;
#20015=DIRECTION ( 'NONE',  ( -0.2306359803922029550, -0.9730401042858035643, 4.741332172907960602E-18 ) ) ;
#20022=ORIENTED_EDGE ( 'NONE', *, *, #9060, .T. ) ;
#20032=VECTOR ( 'NONE', #7857, 999.9999999999998863 ) ;
#20038=CARTESIAN_POINT ( 'NONE',  ( -20.80722593534541076, 19.54644882756858593, -5.432327950763541660E-15 ) ) ;
#20095=ORIENTED_EDGE ( 'NONE', *, *, #9060, .F. ) ;
#20099=EDGE_CURVE ( 'NONE', #1307, #11939, #20183, .T. ) ;
#20183=CIRCLE ( 'NONE', #445, 3.499999999999996891 ) ;
#20258=DIRECTION ( 'NONE',  ( 0.9730401042858036753, -0.2306359803922031493, 2.740969466505752002E-16 ) ) ;
#20261=DIRECTION ( 'NONE',  ( 0.9730401042858036753, -0.2306359803922031493, 2.740969466505752002E-16 ) ) ;
#20269=AXIS2_PLACEMENT_3D ( 'NONE', #17578, #22906, #1511 ) ;
#20274=CARTESIAN_POINT ( 'NONE',  ( -1.437248611304650980, 16.42796209631955051, -7.586732966291266084E-17 ) ) ;
#20283=ORIENTED_EDGE ( 'NONE', *, *, #20431, .T. ) ;
#20311=CARTESIAN_POINT ( 'NONE',  ( -3.458317987535627580, 19.03127855354509990, -7.999999999999998224 ) ) ;
#20363=LINE ( 'NONE', #20828, #7971 ) ;
#20431=EDGE_CURVE ( 'NONE', #4956, #15418, #10748, .T. ) ;
#20566=AXIS2_PLACEMENT_3D ( 'NONE', #15343, #17368, #22808 ) ;
#20717=EDGE_LOOP ( 'NONE', ( #21022, #1628 ) ) ;
#20724=ORIENTED_EDGE ( 'NONE', *, *, #6654, .F. ) ;
#20735=EDGE_CURVE ( 'NONE', #5237, #4833, #4307, .T. ) ;
#20784=AXIS2_PLACEMENT_3D ( 'NONE', #18005, #21654, #16316 ) ;
#20828=CARTESIAN_POINT ( 'NONE',  ( -5.657453702850906652, 21.67680139518235549, -1.552841462206820572E-15 ) ) ;
#20850=CIRCLE ( 'NONE', #10269, 7.999999999999997335 ) ;
#20868=( GEOMETRIC_REPRESENTATION_CONTEXT ( 3 ) GLOBAL_UNCERTAINTY_ASSIGNED_CONTEXT ( ( #12981 ) ) GLOBAL_UNIT_ASSIGNED_CONTEXT ( ( #2012, #1358, #21196 ) ) REPRESENTATION_CONTEXT ( 'NONE', 'WORKASPACE' ) );
#20901=LINE ( 'NONE', #12134, #11647 ) ;
#20914=CARTESIAN_POINT ( 'NONE',  ( -20.80722593534541076, 19.54644882756858948, 2.500000000000000000 ) ) ;
#20921=ORIENTED_EDGE ( 'NONE', *, *, #7613, .T. ) ;
#20946=DIRECTION ( 'NONE',  ( -1.248400535696349791E-16, 3.446306084657139973E-17, 1.000000000000000000 ) ) ;
#20957=DIRECTION ( 'NONE',  ( -0.2306359803922029550, -0.9730401042858035643, 4.741332172907960602E-18 ) ) ;
#21019=ORIENTED_EDGE ( 'NONE', *, *, #18742, .F. ) ;
#21022=ORIENTED_EDGE ( 'NONE', *, *, #20099, .T. ) ;
#21196=( NAMED_UNIT ( * ) SI_UNIT ( $, .STERADIAN. ) SOLID_ANGLE_UNIT ( ) );
#21200=DIRECTION ( 'NONE',  ( 0.000000000000000000, 1.000000000000000000, 0.000000000000000000 ) ) ;
#21204=CIRCLE ( 'NONE', #3388, 7.999999999999998224 ) ;
#21240=VERTEX_POINT ( 'NONE', #21854 ) ;
#21242=LINE ( 'NONE', #14127, #2365 ) ;
#21256=DIRECTION ( 'NONE',  ( -0.9730401042858033422, 0.2306359803922031215, -1.141364251305443211E-16 ) ) ;
#21259=ORIENTED_EDGE ( 'NONE', *, *, #2005, .F. ) ;
#21313=CARTESIAN_POINT ( 'NONE',  ( -6.134178274321590685, 19.66552749962360025, -1.543041128605420056E-15 ) ) ;
#21330=AXIS2_PLACEMENT_3D ( 'NONE', #10135, #13807, #6562 ) ;
#21341=DIRECTION ( 'NONE',  ( -1.248400535696349791E-16, 3.446306084657144903E-17, 1.000000000000000000 ) ) ;
#21392=CARTESIAN_POINT ( 'NONE',  ( -11.25243430249432386, 23.00295828243753249, -3.128898905447639338E-15 ) ) ;
#21433=DIRECTION ( 'NONE',  ( 0.9730401042858035643, -0.2306359803922028717, 2.740969466505749044E-16 ) ) ;
#21457=CARTESIAN_POINT ( 'NONE',  ( -12.93765415188440038, 21.27812940799834962, -3.459521196011834845E-15 ) ) ;
#21481=DIRECTION ( 'NONE',  ( -0.2306359803922031215, -0.9730401042858035643, 4.741332172907962143E-18 ) ) ;
#21572=ORIENTED_EDGE ( 'NONE', *, *, #13009, .F. ) ;
#21573=PLANE ( 'NONE',  #9778 ) ;
#21608=DIRECTION ( 'NONE',  ( 0.9730401042858036753, -0.2306359803922031493, 2.740969466505752002E-16 ) ) ;
#21654=DIRECTION ( 'NONE',  ( 0.9730401042858036753, -0.2306359803922031493, 2.740969466505752002E-16 ) ) ;
#21672=ADVANCED_FACE ( 'NONE', ( #7925 ), #4424, .F. ) ;
#21699=DIRECTION ( 'NONE',  ( 4.063875459488300452E-16, -1.011971878839181895E-16, -1.000000000000000000 ) ) ;
#21781=DIRECTION ( 'NONE',  ( 0.9730401042858036753, -0.2306359803922028995, 2.740969466505749537E-16 ) ) ;
#21793=FACE_OUTER_BOUND ( 'NONE', #11371, .T. ) ;
#21841=FACE_OUTER_BOUND ( 'NONE', #3076, .T. ) ;
#21854=CARTESIAN_POINT ( 'NONE',  ( -25.65326162860803194, 22.49081825942809942, -2.500000000000000888 ) ) ;
#21880=DIRECTION ( 'NONE',  ( 0.9730401042858036753, -0.2306359803922031493, 2.740969466505752002E-16 ) ) ;
#22166=CARTESIAN_POINT ( 'NONE',  ( -0.9605240398339689456, 18.43923599187829865, -8.566766326431390468E-17 ) ) ;
#22191=DIRECTION ( 'NONE',  ( 0.2306359803922031215, 0.9730401042858034533, -4.741332172907939802E-18 ) ) ;
#22241=CARTESIAN_POINT ( 'NONE',  ( 1.213484035536889882, 25.73383521926719908, -2.500000000000000000 ) ) ;
#22268=EDGE_LOOP ( 'NONE', ( #17288, #17810, #12215, #17795, #15458 ) ) ;
#22316=ADVANCED_FACE ( 'NONE', ( #18001 ), #16090, .T. ) ;
#22354=ADVANCED_FACE ( 'NONE', ( #1587 ), #14069, .F. ) ;
#22371=ORIENTED_EDGE ( 'NONE', *, *, #14014, .F. ) ;
#22405=CARTESIAN_POINT ( 'NONE',  ( -18.05391955182270181, 22.49081825942809942, -4.900728725074969882E-15 ) ) ;
#22465=VERTEX_POINT ( 'NONE', #19999 ) ;
#22478=DIRECTION ( 'NONE',  ( 0.9730401042858033422, -0.2306359803922031215, 3.994774879569051239E-16 ) ) ;
#22490=LINE ( 'NONE', #22241, #1283 ) ;
#22506=ORIENTED_EDGE ( 'NONE', *, *, #12336, .F. ) ;
#22517=DIRECTION ( 'NONE',  ( -0.2306359803922028995, -0.9730401042858034533, 4.741332172907957521E-18 ) ) ;
#22554=ORIENTED_EDGE ( 'NONE', *, *, #15631, .T. ) ;
#22604=CARTESIAN_POINT ( 'NONE',  ( -16.30123784160759826, 29.88528286632680064, 2.500000000000000000 ) ) ;
#22662=VERTEX_POINT ( 'NONE', #863 ) ;
#22663=VERTEX_POINT ( 'NONE', #2779 ) ;
#22695=ORIENTED_EDGE ( 'NONE', *, *, #3323, .F. ) ;
#22706=MECHANICAL_CONTEXT ( 'NONE', #3050, 'mechanical' ) ;
#22808=DIRECTION ( 'NONE',  ( 1.000000000000000000, 0.000000000000000000, 0.000000000000000000 ) ) ;
#22823=DIRECTION ( 'NONE',  ( 0.2306359803922030938, 0.9730401042858035643, -4.741332172907964454E-18 ) ) ;
#22856=CARTESIAN_POINT ( 'NONE',  ( -19.80660126203780180, 15.09635365252939998, 2.500000000000000000 ) ) ;
#22906=DIRECTION ( 'NONE',  ( 0.9730401042858035643, -0.2306359803922028717, 2.025546614365803772E-16 ) ) ;
#22907=EDGE_LOOP ( 'NONE', ( #8219, #23076 ) ) ;
#22913=ORIENTED_EDGE ( 'NONE', *, *, #3617, .T. ) ;
#22929=DIRECTION ( 'NONE',  ( 0.9730401042858035643, -0.2306359803922028717, 2.740969466505750030E-16 ) ) ;
#23020=ORIENTED_EDGE ( 'NONE', *, *, #7454, .F. ) ;
#23070=ORIENTED_EDGE ( 'NONE', *, *, #2845, .T. ) ;
#23076=ORIENTED_EDGE ( 'NONE', *, *, #3873, .F. ) ;
#23079=DIRECTION ( 'NONE',  ( 0.2306359803922028995, 0.9730401042858035643, -4.741332172907957521E-18 ) ) ;
#23082=DIRECTION ( 'NONE',  ( -0.9730401042858036753, 0.2306359803922028995, -2.740969466505749537E-16 ) ) ;
#23133=DIRECTION ( 'NONE',  ( -0.2306359803922032603, -0.9730401042858035643, 4.741332172907965995E-18 ) ) ;
#23182=DIRECTION ( 'NONE',  ( 1.000000000000000000, 1.248400535696349791E-16, 5.473822126268819266E-49 ) ) ;
#23304=DIRECTION ( 'NONE',  ( 4.063875459488295522E-16, -1.011971878839177951E-16, -1.000000000000000000 ) ) ;
#23343=EDGE_LOOP ( 'NONE', ( #19586, #3538, #2558, #15613, #4966, #20022, #20724, #12573, #19602 ) ) ;
#23374=CIRCLE ( 'NONE', #18090, 2.066999999999997062 ) ;
#23454=DIRECTION ( 'NONE',  ( 0.9730401042858035643, -0.2306359803922028717, 6.356122819266969852E-16 ) ) ;
#23515=COLOUR_RGB('Deep Blue', 0.09019608, 0.27058824, 0.51372549);
#23516=FILL_AREA_STYLE_COLOUR('',#23515);
#23517=FILL_AREA_STYLE('',(#23516));
#23518=SURFACE_STYLE_FILL_AREA(#23517);
#23519=SURFACE_SIDE_STYLE('',(#23518));
#23520=SURFACE_STYLE_USAGE(.BOTH.,#23519);
#23521=PRESENTATION_STYLE_ASSIGNMENT((#23520));
#23609=STYLED_ITEM('',(#23521),#17699);
#23610=MECHANICAL_DESIGN_GEOMETRIC_PRESENTATION_REPRESENTATION('',(#23609),#20868);
ENDSEC;
END-ISO-10303-21;
